ISO-10303-21;
HEADER;
FILE_DESCRIPTION (('STEP AP214'),
    '1' );
FILE_NAME ('socket head cap screw_iso_ISO 4762 M4 x 30 - 20N.step',
    '2026-09-29T11:11:29',
    ( '' ),
    ( '' ),
    'SwSTEP 2.0',
    'SolidWorks 2026',
    '' );
FILE_SCHEMA (( 'AUTOMOTIVE_DESIGN' ));
ENDSEC;

DATA;
#1=EDGE_CURVE ( 'NONE', #3439, #1476, #1309, .T. ) ;
#3=AXIS2_PLACEMENT_3D ( 'NONE', #1406, #4531, #6990 ) ;
#12=DIRECTION ( 'NONE',  ( 1.000000000000000000, 0.000000000000000000, 0.000000000000000000 ) ) ;
#22=ORIENTED_EDGE ( 'NONE', *, *, #6310, .F. ) ;
#65=ORIENTED_EDGE ( 'NONE', *, *, #4888, .T. ) ;
#69=FACE_OUTER_BOUND ( 'NONE', #3093, .T. ) ;
#89=CIRCLE ( 'NONE', #1214, 3.500000000000000000 ) ;
#94=VERTEX_POINT ( 'NONE', #8292 ) ;
#95=DIRECTION ( 'NONE',  ( 0.000000000000000000, 0.000000000000000000, -1.000000000000000000 ) ) ;
#135=CIRCLE ( 'NONE', #6335, 3.299999999999999822 ) ;
#136=CARTESIAN_POINT ( 'NONE',  ( 0.000000000000000000, 0.8865213383406683745, -1.535500000000000753 ) ) ;
#137=EDGE_CURVE ( 'NONE', #5904, #1249, #6293, .T. ) ;
#141=DIRECTION ( 'NONE',  ( 0.000000000000000000, 0.000000000000000000, 1.000000000000000000 ) ) ;
#152=ORIENTED_EDGE ( 'NONE', *, *, #4060, .F. ) ;
#166=EDGE_LOOP ( 'NONE', ( #6634, #5758, #5300, #3325 ) ) ;
#186=STYLED_ITEM ( 'NONE', ( #5619 ), #2959 ) ;
#188=EDGE_CURVE ( 'NONE', #5393, #2290, #961, .T. ) ;
#202=SURFACE_STYLE_FILL_AREA ( #243 ) ;
#216=LINE ( 'NONE', #4229, #1862 ) ;
#243=FILL_AREA_STYLE ('',( #6897 ) ) ;
#248=FACE_OUTER_BOUND ( 'NONE', #8420, .T. ) ;
#255=DIRECTION ( 'NONE',  ( -1.000000000000000000, -0.000000000000000000, -0.000000000000000000 ) ) ;
#263=VECTOR ( 'NONE', #3964, 1000.000000000000227 ) ;
#287=( NAMED_UNIT ( * ) SI_UNIT ( $, .STERADIAN. ) SOLID_ANGLE_UNIT ( ) );
#292=FACE_OUTER_BOUND ( 'NONE', #3738, .T. ) ;
#297=EDGE_LOOP ( 'NONE', ( #7716, #333, #3919, #4177, #5787 ) ) ;
#322=EDGE_LOOP ( 'NONE', ( #8677, #7395, #7387, #6062 ) ) ;
#323=ORIENTED_EDGE ( 'NONE', *, *, #6329, .F. ) ;
#333=ORIENTED_EDGE ( 'NONE', *, *, #6376, .F. ) ;
#335=AXIS2_PLACEMENT_3D ( 'NONE', #4090, #3522, #8324 ) ;
#344=VERTEX_POINT ( 'NONE', #379 ) ;
#370=CARTESIAN_POINT ( 'NONE',  ( -31.74999999999995737, 0.000000000000000000, 2.000000000000000888 ) ) ;
#376=TOROIDAL_SURFACE ( 'NONE', #3209, 2.200000000000001066, 0.2000000000000000111 ) ;
#379=CARTESIAN_POINT ( 'NONE',  ( 2.886521338340684917, 1.601138781673192758E-19, 0.000000000000000000 ) ) ;
#385=ORIENTED_EDGE ( 'NONE', *, *, #4770, .T. ) ;
#392=FACE_OUTER_BOUND ( 'NONE', #2100, .T. ) ;
#394=DIRECTION ( 'NONE',  ( -1.000000000000000000, -0.000000000000000000, -0.000000000000000000 ) ) ;
#405=DIRECTION ( 'NONE',  ( 0.000000000000000000, -0.8660254037844390407, -0.4999999999999992784 ) ) ;
#413=ADVANCED_FACE ( 'NONE', ( #392 ), #7895, .T. ) ;
#418=DIRECTION ( 'NONE',  ( 0.000000000000000000, 0.000000000000000000, 1.000000000000000000 ) ) ;
#428=EDGE_CURVE ( 'NONE', #5205, #1907, #5881, .T. ) ;
#432=CARTESIAN_POINT ( 'NONE',  ( 4.000000000000003553, 0.000000000000000000, 0.000000000000000000 ) ) ;
#439=AXIS2_PLACEMENT_3D ( 'NONE', #6686, #1307, #1061 ) ;
#456=ORIENTED_EDGE ( 'NONE', *, *, #629, .F. ) ;
#465=EDGE_CURVE ( 'NONE', #4613, #1975, #7431, .T. ) ;
#474=LINE ( 'NONE', #7771, #1262 ) ;
#497=ORIENTED_EDGE ( 'NONE', *, *, #3286, .F. ) ;
#510=ORIENTED_EDGE ( 'NONE', *, *, #7673, .F. ) ;
#532=PLANE ( 'NONE',  #3808 ) ;
#568=CARTESIAN_POINT ( 'NONE',  ( 33.61000000000001364, 0.000000000000000000, 0.000000000000000000 ) ) ;
#577=DIRECTION ( 'NONE',  ( -1.000000000000000000, -0.000000000000000000, -0.000000000000000000 ) ) ;
#587=CIRCLE ( 'NONE', #335, 2.200000000000001066 ) ;
#606=ADVANCED_FACE ( 'NONE', ( #2522, #3714 ), #3797, .T. ) ;
#610=CARTESIAN_POINT ( 'NONE',  ( 34.00000000000000000, 0.000000000000000000, 0.000000000000000000 ) ) ;
#612=EDGE_CURVE ( 'NONE', #7038, #4661, #5452, .T. ) ;
#629=EDGE_CURVE ( 'NONE', #4891, #8357, #1533, .T. ) ;
#646=EDGE_LOOP ( 'NONE', ( #7860, #1088, #1174 ) ) ;
#651=CARTESIAN_POINT ( 'NONE',  ( -31.74999999999995737, 4.286263797015736595E-16, -3.500000000000000000 ) ) ;
#663=AXIS2_PLACEMENT_3D ( 'NONE', #432, #3150, #5826 ) ;
#704=LINE ( 'NONE', #2703, #2722 ) ;
#717=ORIENTED_EDGE ( 'NONE', *, *, #3971, .F. ) ;
#722=STYLED_ITEM ( 'NONE', ( #1742 ), #4644 ) ;
#730=CARTESIAN_POINT ( 'NONE',  ( 2.000000000000000000, 1.773042676681340968, -1.951563910473907981E-15 ) ) ;
#737=AXIS2_PLACEMENT_3D ( 'NONE', #1807, #7132, #4488 ) ;
#750=CARTESIAN_POINT ( 'NONE',  ( 2.000000000000000000, -1.314525273895014276E-15, -1.535500000000000087 ) ) ;
#751=AXIS2_PLACEMENT_3D ( 'NONE', #3944, #577, #5339 ) ;
#761=CARTESIAN_POINT ( 'NONE',  ( 34.00000000000000000, 0.000000000000000000, 0.000000000000000000 ) ) ;
#777=CARTESIAN_POINT ( 'NONE',  ( 0.1999999999999987899, 0.000000000000000000, 0.000000000000000000 ) ) ;
#783=ORIENTED_EDGE ( 'NONE', *, *, #3043, .F. ) ;
#792=TOROIDAL_SURFACE ( 'NONE', #4457, 3.299999999999999822, 0.2000000000000000111 ) ;
#810=ORIENTED_EDGE ( 'NONE', *, *, #4569, .F. ) ;
#827=ORIENTED_EDGE ( 'NONE', *, *, #612, .F. ) ;
#839=DIRECTION ( 'NONE',  ( 0.000000000000000000, -1.000000000000000000, 8.560894001270036306E-16 ) ) ;
#844=AXIS2_PLACEMENT_3D ( 'NONE', #761, #1599, #2184 ) ;
#848=CARTESIAN_POINT ( 'NONE',  ( 2.000000000000000000, -1.329782007511005837, 0.7677500000000023750 ) ) ;
#863=DIRECTION ( 'NONE',  ( 1.000000000000000000, 0.000000000000000000, 0.000000000000000000 ) ) ;
#898=DIRECTION ( 'NONE',  ( 0.000000000000000000, 0.8660254037844380415, -0.5000000000000012212 ) ) ;
#899=VERTEX_POINT ( 'NONE', #5351 ) ;
#929=ADVANCED_FACE ( 'NONE', ( #6725 ), #3255, .F. ) ;
#933=DIRECTION ( 'NONE',  ( -0.000000000000000000, 1.000000000000000000, 1.224646799147353207E-16 ) ) ;
#941=CARTESIAN_POINT ( 'NONE',  ( 2.000000000000000000, 1.773042676681340968, -1.951563910473907981E-15 ) ) ;
#942=ORIENTED_EDGE ( 'NONE', *, *, #4836, .T. ) ;
#961=LINE ( 'NONE', #3740, #2648 ) ;
#966=ADVANCED_FACE ( 'NONE', ( #7257 ), #6764, .T. ) ;
#976=LINE ( 'NONE', #7930, #6829 ) ;
#979=DIRECTION ( 'NONE',  ( 0.000000000000000000, 1.000000000000000000, -1.467581828789149335E-15 ) ) ;
#990=PRODUCT_DEFINITION_SHAPE ( 'NONE', 'NONE',  #1843 ) ;
#1028=( LENGTH_UNIT ( ) NAMED_UNIT ( * ) SI_UNIT ( .MILLI., .METRE. ) );
#1041=FACE_BOUND ( 'NONE', #3210, .T. ) ;
#1042=ORIENTED_EDGE ( 'NONE', *, *, #7811, .T. ) ;
#1061=DIRECTION ( 'NONE',  ( 0.000000000000000000, 0.000000000000000000, 1.000000000000000000 ) ) ;
#1063=DIRECTION ( 'NONE',  ( -0.000000000000000000, 0.8660254037844392627, 0.4999999999999990008 ) ) ;
#1071=EDGE_CURVE ( 'NONE', #5205, #5875, #6198, .T. ) ;
#1080=CARTESIAN_POINT ( 'NONE',  ( 2.000000000000000000, 1.773042676681340968, -1.951563910473907981E-15 ) ) ;
#1088=ORIENTED_EDGE ( 'NONE', *, *, #6329, .T. ) ;
#1107=CARTESIAN_POINT ( 'NONE',  ( 4.200000000000001954, 2.694222958124178486E-16, 2.200000000000001066 ) ) ;
#1123=AXIS2_PLACEMENT_3D ( 'NONE', #1080, #405, #3774 ) ;
#1132=DIRECTION ( 'NONE',  ( -1.000000000000000000, -0.000000000000000000, -0.000000000000000000 ) ) ;
#1140=ORIENTED_EDGE ( 'NONE', *, *, #8599, .F. ) ;
#1149=CARTESIAN_POINT ( 'NONE',  ( 2.000000000000000000, -0.8865213383406692627, 1.535500000000001641 ) ) ;
#1155=CIRCLE ( 'NONE', #7353, 1.535500000000000087 ) ;
#1174=ORIENTED_EDGE ( 'NONE', *, *, #6666, .F. ) ;
#1199=CIRCLE ( 'NONE', #2764, 1.535500000000000087 ) ;
#1209=VERTEX_POINT ( 'NONE', #3102 ) ;
#1213=ORIENTED_EDGE ( 'NONE', *, *, #4836, .F. ) ;
#1214=AXIS2_PLACEMENT_3D ( 'NONE', #777, #863, #6858 ) ;
#1217=LINE ( 'NONE', #3913, #4688 ) ;
#1222=CIRCLE ( 'NONE', #3351, 1.535500000000000087 ) ;
#1232=ADVANCED_FACE ( 'NONE', ( #5783 ), #2079, .T. ) ;
#1245=CARTESIAN_POINT ( 'NONE',  ( 2.000000000000000000, 1.773042676681340968, -1.951563910473907981E-15 ) ) ;
#1249=VERTEX_POINT ( 'NONE', #2443 ) ;
#1262=VECTOR ( 'NONE', #5697, 1000.000000000000000 ) ;
#1271=VECTOR ( 'NONE', #2457, 1000.000000000000114 ) ;
#1274=ADVANCED_FACE ( 'NONE', ( #5642 ), #5030, .F. ) ;
#1286=LINE ( 'NONE', #4737, #2691 ) ;
#1296=ORIENTED_EDGE ( 'NONE', *, *, #7973, .T. ) ;
#1307=DIRECTION ( 'NONE',  ( -1.000000000000000000, -0.000000000000000000, -0.000000000000000000 ) ) ;
#1309=LINE ( 'NONE', #7355, #263 ) ;
#1314=CARTESIAN_POINT ( 'NONE',  ( 2.000000000000000000, -0.8865213383406692627, 1.535500000000001641 ) ) ;
#1320=DIRECTION ( 'NONE',  ( -1.000000000000000000, -0.000000000000000000, -0.000000000000000000 ) ) ;
#1328=CARTESIAN_POINT ( 'NONE',  ( 34.00000000000000000, 2.210487472460973191E-16, -1.610000000000000098 ) ) ;
#1336=DIRECTION ( 'NONE',  ( 0.000000000000000000, 0.000000000000000000, -1.000000000000000000 ) ) ;
#1341=ORIENTED_EDGE ( 'NONE', *, *, #2126, .F. ) ;
#1353=ADVANCED_FACE ( 'NONE', ( #7536 ), #4369, .T. ) ;
#1359=DIRECTION ( 'NONE',  ( 0.000000000000000000, -1.000000000000000000, 1.467581828789149532E-15 ) ) ;
#1361=VECTOR ( 'NONE', #1439, 1000.000000000000000 ) ;
#1367=CARTESIAN_POINT ( 'NONE',  ( 2.000000000000000000, -1.773042676681341634, 2.493664996716660198E-15 ) ) ;
#1406=CARTESIAN_POINT ( 'NONE',  ( -31.74999999999995737, 0.000000000000000000, 0.000000000000000000 ) ) ;
#1414=VECTOR ( 'NONE', #6780, 1000.000000000000000 ) ;
#1432=( GEOMETRIC_REPRESENTATION_CONTEXT ( 3 ) GLOBAL_UNCERTAINTY_ASSIGNED_CONTEXT ( ( #5029 ) ) GLOBAL_UNIT_ASSIGNED_CONTEXT ( ( #3763, #3106, #5786 ) ) REPRESENTATION_CONTEXT ( 'NONE', 'WORKASPACE' ) );
#1439=DIRECTION ( 'NONE',  ( -1.000000000000000000, -0.000000000000000000, -0.000000000000000000 ) ) ;
#1441=CARTESIAN_POINT ( 'NONE',  ( 4.000000000000003553, 0.000000000000000000, 3.500000000000000000 ) ) ;
#1447=CIRCLE ( 'NONE', #2579, 1.535500000000000087 ) ;
#1460=ORIENTED_EDGE ( 'NONE', *, *, #3286, .T. ) ;
#1461=DIRECTION ( 'NONE',  ( 0.000000000000000000, 0.000000000000000000, 1.000000000000000000 ) ) ;
#1466=LINE ( 'NONE', #3507, #6194 ) ;
#1470=ORIENTED_EDGE ( 'NONE', *, *, #8697, .T. ) ;
#1476=VERTEX_POINT ( 'NONE', #2201 ) ;
#1491=DIRECTION ( 'NONE',  ( -1.000000000000000000, -0.000000000000000000, -0.000000000000000000 ) ) ;
#1515=ORIENTED_EDGE ( 'NONE', *, *, #137, .F. ) ;
#1533=LINE ( 'NONE', #4853, #6721 ) ;
#1551=CARTESIAN_POINT ( 'NONE',  ( 0.000000000000000000, 1.773042676681340968, -1.951563910473907981E-15 ) ) ;
#1557=CARTESIAN_POINT ( 'NONE',  ( 2.000000000000000000, -0.8865213383406692627, 1.535500000000001641 ) ) ;
#1569=ORIENTED_EDGE ( 'NONE', *, *, #6881, .T. ) ;
#1574=EDGE_CURVE ( 'NONE', #4958, #94, #89, .T. ) ;
#1585=AXIS2_PLACEMENT_3D ( 'NONE', #8295, #1491, #2256 ) ;
#1599=DIRECTION ( 'NONE',  ( -1.000000000000000000, -0.000000000000000000, -0.000000000000000000 ) ) ;
#1611=SURFACE_STYLE_USAGE ( .BOTH. , #3519 ) ;
#1628=PRODUCT ( 'socket head cap screw_iso_ISO 4762 M4 x 30 - 20N', 'socket head cap screw_iso_ISO 4762 M4 x 30 - 20N', '', ( #5555 ) ) ;
#1631=AXIS2_PLACEMENT_3D ( 'NONE', #6294, #255, #418 ) ;
#1633=DIRECTION ( 'NONE',  ( 0.000000000000000000, 0.000000000000000000, 1.000000000000000000 ) ) ;
#1650=ORIENTED_EDGE ( 'NONE', *, *, #3971, .T. ) ;
#1658=( NAMED_UNIT ( * ) PLANE_ANGLE_UNIT ( ) SI_UNIT ( $, .RADIAN. ) );
#1662=CARTESIAN_POINT ( 'NONE',  ( 2.000000000000000000, 0.000000000000000000, 1.535500000000000087 ) ) ;
#1686=VECTOR ( 'NONE', #3151, 1000.000000000000000 ) ;
#1693=SURFACE_STYLE_FILL_AREA ( #7773 ) ;
#1707=DIRECTION ( 'NONE',  ( 0.000000000000000000, 0.000000000000000000, 1.000000000000000000 ) ) ;
#1734=CIRCLE ( 'NONE', #7079, 1.535500000000000087 ) ;
#1742=PRESENTATION_STYLE_ASSIGNMENT (( #8356 ) ) ;
#1790=CARTESIAN_POINT ( 'NONE',  ( 2.000000000000000000, 0.8865213383406683745, -1.535500000000000753 ) ) ;
#1795=VERTEX_POINT ( 'NONE', #8612 ) ;
#1800=AXIS2_PLACEMENT_3D ( 'NONE', #8129, #2664, #95 ) ;
#1807=CARTESIAN_POINT ( 'NONE',  ( 4.200000000000001954, 0.000000000000000000, 0.000000000000000000 ) ) ;
#1812=EDGE_CURVE ( 'NONE', #3910, #2290, #1912, .T. ) ;
#1821=DIRECTION ( 'NONE',  ( 0.000000000000000000, -1.000000000000000000, 8.560894001270036306E-16 ) ) ;
#1843=PRODUCT_DEFINITION ( 'UNKNOWN', '', #6919, #7580 ) ;
#1844=ORIENTED_EDGE ( 'NONE', *, *, #5468, .T. ) ;
#1852=ORIENTED_EDGE ( 'NONE', *, *, #1071, .F. ) ;
#1856=EDGE_LOOP ( 'NONE', ( #3697, #6178 ) ) ;
#1862=VECTOR ( 'NONE', #8209, 999.9999999999998863 ) ;
#1891=DIRECTION ( 'NONE',  ( 0.000000000000000000, 0.000000000000000000, 1.000000000000000000 ) ) ;
#1906=DIRECTION ( 'NONE',  ( 0.000000000000000000, -0.4999999999999992784, 0.8660254037844389297 ) ) ;
#1907=VERTEX_POINT ( 'NONE', #5379 ) ;
#1912=LINE ( 'NONE', #7949, #2782 ) ;
#1913=DIRECTION ( 'NONE',  ( 0.000000000000000000, 0.000000000000000000, 1.000000000000000000 ) ) ;
#1923=AXIS2_PLACEMENT_3D ( 'NONE', #7383, #2763, #1336 ) ;
#1932=CARTESIAN_POINT ( 'NONE',  ( 2.000000000000000000, 1.773042676681340968, -1.951563910473907981E-15 ) ) ;
#1938=ORIENTED_EDGE ( 'NONE', *, *, #7844, .F. ) ;
#1948=LINE ( 'NONE', #4503, #6931 ) ;
#1957=DIRECTION ( 'NONE',  ( -1.000000000000000000, -0.000000000000000000, -0.000000000000000000 ) ) ;
#1975=VERTEX_POINT ( 'NONE', #7631 ) ;
#1985=LINE ( 'NONE', #651, #1414 ) ;
#2025=CIRCLE ( 'NONE', #4694, 3.500000000000000000 ) ;
#2027=ORIENTED_EDGE ( 'NONE', *, *, #7899, .T. ) ;
#2063=DIRECTION ( 'NONE',  ( -1.000000000000000000, -0.000000000000000000, -0.000000000000000000 ) ) ;
#2065=DIRECTION ( 'NONE',  ( -1.000000000000000000, -0.000000000000000000, -0.000000000000000000 ) ) ;
#2079=TOROIDAL_SURFACE ( 'NONE', #6998, 3.299999999999999822, 0.2000000000000000111 ) ;
#2080=EDGE_CURVE ( 'NONE', #8009, #3178, #1199, .T. ) ;
#2090=AXIS2_PLACEMENT_3D ( 'NONE', #8601, #2568, #6479 ) ;
#2097=DIRECTION ( 'NONE',  ( 0.000000000000000000, 0.000000000000000000, -1.000000000000000000 ) ) ;
#2100=EDGE_LOOP ( 'NONE', ( #717, #1515, #1460, #4122, #4292 ) ) ;
#2113=DIRECTION ( 'NONE',  ( -1.000000000000000000, -0.000000000000000000, -0.000000000000000000 ) ) ;
#2115=ORIENTED_EDGE ( 'NONE', *, *, #5667, .F. ) ;
#2118=ORIENTED_EDGE ( 'NONE', *, *, #4689, .F. ) ;
#2126=EDGE_CURVE ( 'NONE', #94, #4958, #6129, .T. ) ;
#2127=CARTESIAN_POINT ( 'NONE',  ( 34.00000000000000000, 0.000000000000000000, 1.610000000000000098 ) ) ;
#2144=CARTESIAN_POINT ( 'NONE',  ( 2.000000000000000000, 1.329782007511004505, -0.7677500000000018199 ) ) ;
#2179=CARTESIAN_POINT ( 'NONE',  ( 0.000000000000000000, 0.000000000000000000, 0.000000000000000000 ) ) ;
#2184=DIRECTION ( 'NONE',  ( 0.000000000000000000, 0.000000000000000000, 1.000000000000000000 ) ) ;
#2188=DIRECTION ( 'NONE',  ( 0.000000000000000000, 0.000000000000000000, 1.000000000000000000 ) ) ;
#2201=CARTESIAN_POINT ( 'NONE',  ( 2.000000000000000000, 1.329782007511006503, 0.7677499999999991553 ) ) ;
#2250=ORIENTED_EDGE ( 'NONE', *, *, #188, .F. ) ;
#2256=DIRECTION ( 'NONE',  ( 0.000000000000000000, 0.000000000000000000, 1.000000000000000000 ) ) ;
#2258=ORIENTED_EDGE ( 'NONE', *, *, #1812, .T. ) ;
#2287=DIRECTION ( 'NONE',  ( 0.000000000000000000, 0.000000000000000000, -1.000000000000000000 ) ) ;
#2290=VERTEX_POINT ( 'NONE', #7013 ) ;
#2305=EDGE_CURVE ( 'NONE', #8625, #1907, #976, .T. ) ;
#2315=AXIS2_PLACEMENT_3D ( 'NONE', #2179, #2840, #141 ) ;
#2355=FACE_OUTER_BOUND ( 'NONE', #3951, .T. ) ;
#2366=ORIENTED_EDGE ( 'NONE', *, *, #3395, .T. ) ;
#2430=ORIENTED_EDGE ( 'NONE', *, *, #188, .T. ) ;
#2439=DIRECTION ( 'NONE',  ( -1.000000000000000000, -0.000000000000000000, -0.000000000000000000 ) ) ;
#2443=CARTESIAN_POINT ( 'NONE',  ( 0.000000000000000000, -1.773042676681341634, 2.493664996716660198E-15 ) ) ;
#2444=LINE ( 'NONE', #1149, #5034 ) ;
#2457=DIRECTION ( 'NONE',  ( 0.000000000000000000, 0.4999999999999989453, -0.8660254037844392627 ) ) ;
#2469=ADVANCED_FACE ( 'NONE', ( #2916 ), #4304, .F. ) ;
#2473=ORIENTED_EDGE ( 'NONE', *, *, #2678, .F. ) ;
#2500=EDGE_LOOP ( 'NONE', ( #1042, #7341, #4078, #1650, #6553, #5001 ) ) ;
#2507=ORIENTED_EDGE ( 'NONE', *, *, #4845, .T. ) ;
#2515=AXIS2_PLACEMENT_3D ( 'NONE', #3841, #1063, #7813 ) ;
#2522=FACE_BOUND ( 'NONE', #2500, .T. ) ;
#2548=EDGE_CURVE ( 'NONE', #5875, #4340, #4411, .T. ) ;
#2554=AXIS2_PLACEMENT_3D ( 'NONE', #7787, #1707, #3692 ) ;
#2568=DIRECTION ( 'NONE',  ( -1.000000000000000000, 0.000000000000000000, -0.000000000000000000 ) ) ;
#2579=AXIS2_PLACEMENT_3D ( 'NONE', #8632, #2065, #1891 ) ;
#2614=DIRECTION ( 'NONE',  ( 0.000000000000000000, 0.000000000000000000, 1.000000000000000000 ) ) ;
#2621=EDGE_CURVE ( 'NONE', #7038, #4958, #7171, .T. ) ;
#2623=PLANE ( 'NONE',  #7136 ) ;
#2625=DIRECTION ( 'NONE',  ( 0.000000000000000000, 0.000000000000000000, 1.000000000000000000 ) ) ;
#2630=PLANE ( 'NONE',  #6651 ) ;
#2645=VECTOR ( 'NONE', #8366, 1000.000000000000114 ) ;
#2648=VECTOR ( 'NONE', #3699, 1000.000000000000000 ) ;
#2664=DIRECTION ( 'NONE',  ( 1.000000000000000000, 0.000000000000000000, 0.000000000000000000 ) ) ;
#2678=EDGE_CURVE ( 'NONE', #8357, #1249, #1217, .T. ) ;
#2691=VECTOR ( 'NONE', #4075, 1000.000000000000114 ) ;
#2702=LINE ( 'NONE', #1367, #4611 ) ;
#2703=CARTESIAN_POINT ( 'NONE',  ( 2.000000000000000000, 1.880445160090761061E-16, -1.535500000000000087 ) ) ;
#2717=DIRECTION ( 'NONE',  ( 1.000000000000000000, 0.000000000000000000, 0.000000000000000000 ) ) ;
#2722=VECTOR ( 'NONE', #4021, 1000.000000000000000 ) ;
#2723=EDGE_LOOP ( 'NONE', ( #1341, #8385, #3252, #6587 ) ) ;
#2733=MECHANICAL_DESIGN_GEOMETRIC_PRESENTATION_REPRESENTATION('',(#186),#3155);
#2736=ADVANCED_FACE ( 'NONE', ( #6724 ), #7475, .F. ) ;
#2737=CIRCLE ( 'NONE', #751, 1.610000000000000098 ) ;
#2756=DIRECTION ( 'NONE',  ( -1.000000000000000000, -0.000000000000000000, -0.000000000000000000 ) ) ;
#2763=DIRECTION ( 'NONE',  ( 0.000000000000000000, -1.000000000000000000, 0.000000000000000000 ) ) ;
#2764=AXIS2_PLACEMENT_3D ( 'NONE', #7503, #2756, #3461 ) ;
#2773=AXIS2_PLACEMENT_3D ( 'NONE', #7719, #8342, #4326 ) ;
#2782=VECTOR ( 'NONE', #5290, 999.9999999999998863 ) ;
#2840=DIRECTION ( 'NONE',  ( -1.000000000000000000, -0.000000000000000000, -0.000000000000000000 ) ) ;
#2846=CARTESIAN_POINT ( 'NONE',  ( 2.000000000000000000, -0.8865213383406692627, 1.535500000000001641 ) ) ;
#2849=DIRECTION ( 'NONE',  ( -1.000000000000000000, -0.000000000000000000, -0.000000000000000000 ) ) ;
#2871=CARTESIAN_POINT ( 'NONE',  ( 2.000000000000000000, -1.773042676681341634, 2.493664996716660198E-15 ) ) ;
#2879=DIRECTION ( 'NONE',  ( 1.000000000000000000, 0.000000000000000000, 0.000000000000000000 ) ) ;
#2887=CARTESIAN_POINT ( 'NONE',  ( 0.1999999999999987899, 4.041334437186265510E-16, -3.299999999999999822 ) ) ;
#2916=FACE_OUTER_BOUND ( 'NONE', #4182, .T. ) ;
#2949=CYLINDRICAL_SURFACE ( 'NONE', #3, 2.000000000000000888 ) ;
#2959=MANIFOLD_SOLID_BREP ( 'Hex', #4355 ) ;
#2963=EDGE_CURVE ( 'NONE', #4661, #7038, #2025, .T. ) ;
#2977=CARTESIAN_POINT ( 'NONE',  ( 4.200000000000001954, 0.000000000000000000, 2.000000000000000888 ) ) ;
#2980=FILL_AREA_STYLE_COLOUR ( '', #3828 ) ;
#2981=ORIENTED_EDGE ( 'NONE', *, *, #1, .T. ) ;
#2993=LINE ( 'NONE', #5014, #1271 ) ;
#3011=CARTESIAN_POINT ( 'NONE',  ( 34.00000000000000000, 1.610000000000000098, 0.000000000000000000 ) ) ;
#3034=CARTESIAN_POINT ( 'NONE',  ( 2.000000000000000000, -0.8865213383406692627, 1.535500000000001641 ) ) ;
#3037=LINE ( 'NONE', #370, #7228 ) ;
#3043=EDGE_CURVE ( 'NONE', #6389, #899, #3579, .T. ) ;
#3052=ORIENTED_EDGE ( 'NONE', *, *, #6376, .T. ) ;
#3058=CIRCLE ( 'NONE', #1923, 0.2000000000000000944 ) ;
#3078=DIRECTION ( 'NONE',  ( -1.000000000000000000, -0.000000000000000000, -0.000000000000000000 ) ) ;
#3080=DIRECTION ( 'NONE',  ( -0.5000000000000061062, 0.000000000000000000, 0.8660254037844351549 ) ) ;
#3087=CARTESIAN_POINT ( 'NONE',  ( 4.200000000000001954, 0.000000000000000000, -2.200000000000001066 ) ) ;
#3089=DIRECTION ( 'NONE',  ( -1.000000000000000000, -0.000000000000000000, -0.000000000000000000 ) ) ;
#3093=EDGE_LOOP ( 'NONE', ( #2258, #2250, #3678, #323, #5773 ) ) ;
#3099=CARTESIAN_POINT ( 'NONE',  ( 33.61000000000001364, 0.000000000000000000, 0.000000000000000000 ) ) ;
#3102=CARTESIAN_POINT ( 'NONE',  ( 0.000000000000000000, 0.8865213383406717051, 1.535499999999999199 ) ) ;
#3106=( NAMED_UNIT ( * ) PLANE_ANGLE_UNIT ( ) SI_UNIT ( $, .RADIAN. ) );
#3150=DIRECTION ( 'NONE',  ( -1.000000000000000000, -0.000000000000000000, -0.000000000000000000 ) ) ;
#3151=DIRECTION ( 'NONE',  ( -1.000000000000000000, -0.000000000000000000, -0.000000000000000000 ) ) ;
#3154=( NAMED_UNIT ( * ) PLANE_ANGLE_UNIT ( ) SI_UNIT ( $, .RADIAN. ) );
#3155=( GEOMETRIC_REPRESENTATION_CONTEXT ( 3 ) GLOBAL_UNCERTAINTY_ASSIGNED_CONTEXT ( ( #4471 ) ) GLOBAL_UNIT_ASSIGNED_CONTEXT ( ( #7559, #1658, #287 ) ) REPRESENTATION_CONTEXT ( 'NONE', 'WORKASPACE' ) );
#3178=VERTEX_POINT ( 'NONE', #5259 ) ;
#3209=AXIS2_PLACEMENT_3D ( 'NONE', #3288, #5964, #8083 ) ;
#3210=EDGE_LOOP ( 'NONE', ( #5686, #3847 ) ) ;
#3240=CARTESIAN_POINT ( 'NONE',  ( 2.000000000000000000, 1.773042676681340968, -1.951563910473907981E-15 ) ) ;
#3243=CARTESIAN_POINT ( 'NONE',  ( 4.000000000000001776, 0.000000000000000000, -2.200000000000001066 ) ) ;
#3252=ORIENTED_EDGE ( 'NONE', *, *, #4497, .F. ) ;
#3255=PLANE ( 'NONE',  #4115 ) ;
#3262=ADVANCED_FACE ( 'NONE', ( #3426 ), #2630, .F. ) ;
#3281=DIRECTION ( 'NONE',  ( 0.000000000000000000, 0.000000000000000000, 1.000000000000000000 ) ) ;
#3283=VECTOR ( 'NONE', #5938, 999.9999999999998863 ) ;
#3286=EDGE_CURVE ( 'NONE', #5904, #3178, #5474, .T. ) ;
#3288=CARTESIAN_POINT ( 'NONE',  ( 4.200000000000001954, 0.000000000000000000, 0.000000000000000000 ) ) ;
#3325=ORIENTED_EDGE ( 'NONE', *, *, #2305, .F. ) ;
#3336=CARTESIAN_POINT ( 'NONE',  ( 2.000000000000000000, 1.773042676681340968, -1.951563910473907981E-15 ) ) ;
#3351=AXIS2_PLACEMENT_3D ( 'NONE', #5922, #5380, #1913 ) ;
#3360=APPLICATION_CONTEXT ( 'automotive_design' ) ;
#3394=VERTEX_POINT ( 'NONE', #4698 ) ;
#3395=EDGE_CURVE ( 'NONE', #4958, #899, #3058, .T. ) ;
#3398=ORIENTED_EDGE ( 'NONE', *, *, #7019, .F. ) ;
#3413=DIRECTION ( 'NONE',  ( -1.000000000000000000, -0.000000000000000000, -0.000000000000000000 ) ) ;
#3416=ADVANCED_FACE ( 'NONE', ( #3467 ), #792, .T. ) ;
#3417=AXIS2_PLACEMENT_3D ( 'NONE', #2887, #933, #3626 ) ;
#3425=EDGE_LOOP ( 'NONE', ( #6570, #4915, #3398, #5999 ) ) ;
#3426=FACE_OUTER_BOUND ( 'NONE', #8050, .T. ) ;
#3437=DIRECTION ( 'NONE',  ( 0.000000000000000000, 0.8660254037844380415, -0.5000000000000012212 ) ) ;
#3439=VERTEX_POINT ( 'NONE', #941 ) ;
#3461=DIRECTION ( 'NONE',  ( 0.000000000000000000, 0.000000000000000000, 1.000000000000000000 ) ) ;
#3467=FACE_OUTER_BOUND ( 'NONE', #7873, .T. ) ;
#3507=CARTESIAN_POINT ( 'NONE',  ( 34.00000000000000000, 1.971681346627238735E-16, -1.610000000000000098 ) ) ;
#3519=SURFACE_SIDE_STYLE ('',( #202 ) ) ;
#3522=DIRECTION ( 'NONE',  ( -1.000000000000000000, -0.000000000000000000, -0.000000000000000000 ) ) ;
#3552=VERTEX_POINT ( 'NONE', #7639 ) ;
#3560=DIRECTION ( 'NONE',  ( -1.000000000000000000, -0.000000000000000000, -0.000000000000000000 ) ) ;
#3570=AXIS2_PLACEMENT_3D ( 'NONE', #3087, #5765, #5851 ) ;
#3579=CIRCLE ( 'NONE', #2315, 3.299999999999999822 ) ;
#3626=DIRECTION ( 'NONE',  ( 0.000000000000000000, -1.224646799147353207E-16, 1.000000000000000000 ) ) ;
#3634=AXIS2_PLACEMENT_3D ( 'NONE', #3099, #5242, #4420 ) ;
#3650=ORIENTED_EDGE ( 'NONE', *, *, #5202, .F. ) ;
#3675=LINE ( 'NONE', #7147, #4371 ) ;
#3678=ORIENTED_EDGE ( 'NONE', *, *, #6870, .F. ) ;
#3692=DIRECTION ( 'NONE',  ( 1.000000000000000000, 0.000000000000000000, 0.000000000000000000 ) ) ;
#3697=ORIENTED_EDGE ( 'NONE', *, *, #4497, .T. ) ;
#3699=DIRECTION ( 'NONE',  ( -1.000000000000000000, -0.000000000000000000, -0.000000000000000000 ) ) ;
#3704=EDGE_LOOP ( 'NONE', ( #6202, #7305, #8372, #5769 ) ) ;
#3714=FACE_OUTER_BOUND ( 'NONE', #1856, .T. ) ;
#3716=ADVANCED_FACE ( 'NONE', ( #5612 ), #8271, .T. ) ;
#3734=LINE ( 'NONE', #1662, #3960 ) ;
#3738=EDGE_LOOP ( 'NONE', ( #827, #4111 ) ) ;
#3740=CARTESIAN_POINT ( 'NONE',  ( 2.000000000000000000, 0.8865213383406683745, -1.535500000000000753 ) ) ;
#3745=EDGE_LOOP ( 'NONE', ( #2473, #456, #1844, #7110, #3934 ) ) ;
#3754=FACE_OUTER_BOUND ( 'NONE', #4231, .T. ) ;
#3756=DIRECTION ( 'NONE',  ( 1.000000000000000000, 0.000000000000000000, 0.000000000000000000 ) ) ;
#3763=( LENGTH_UNIT ( ) NAMED_UNIT ( * ) SI_UNIT ( .MILLI., .METRE. ) );
#3774=DIRECTION ( 'NONE',  ( 0.000000000000000000, 0.4999999999999992784, -0.8660254037844390407 ) ) ;
#3797=PLANE ( 'NONE',  #2090 ) ;
#3808=AXIS2_PLACEMENT_3D ( 'NONE', #1245, #12, #2097 ) ;
#3817=ORIENTED_EDGE ( 'NONE', *, *, #7026, .F. ) ;
#3828=COLOUR_RGB ( '', 0.40784314, 0.44705882, 0.49803922) ;
#3831=ORIENTED_EDGE ( 'NONE', *, *, #5667, .T. ) ;
#3841=CARTESIAN_POINT ( 'NONE',  ( 2.000000000000000000, -1.773042676681341634, 2.493664996716660198E-15 ) ) ;
#3847=ORIENTED_EDGE ( 'NONE', *, *, #7026, .T. ) ;
#3861=CARTESIAN_POINT ( 'NONE',  ( 4.000000000000000000, 3.500000000000000000, 0.000000000000000000 ) ) ;
#3885=AXIS2_PLACEMENT_3D ( 'NONE', #3011, #2879, #4988 ) ;
#3901=CARTESIAN_POINT ( 'NONE',  ( -31.74999999999995737, 0.000000000000000000, 0.000000000000000000 ) ) ;
#3910=VERTEX_POINT ( 'NONE', #1551 ) ;
#3913=CARTESIAN_POINT ( 'NONE',  ( 0.000000000000000000, -0.8865213383406692627, 1.535500000000001641 ) ) ;
#3914=CARTESIAN_POINT ( 'NONE',  ( -31.74999999999995737, 0.000000000000000000, 0.000000000000000000 ) ) ;
#3919=ORIENTED_EDGE ( 'NONE', *, *, #4770, .F. ) ;
#3928=EDGE_CURVE ( 'NONE', #5629, #5205, #1466, .T. ) ;
#3934=ORIENTED_EDGE ( 'NONE', *, *, #137, .T. ) ;
#3940=FACE_OUTER_BOUND ( 'NONE', #3425, .T. ) ;
#3944=CARTESIAN_POINT ( 'NONE',  ( 34.00000000000000000, 0.000000000000000000, 0.000000000000000000 ) ) ;
#3946=VECTOR ( 'NONE', #5561, 1000.000000000000000 ) ;
#3951=EDGE_LOOP ( 'NONE', ( #7048, #1470, #1569, #4789, #4579 ) ) ;
#3960=VECTOR ( 'NONE', #3080, 1000.000000000000000 ) ;
#3964=DIRECTION ( 'NONE',  ( 0.000000000000000000, -0.4999999999999992784, 0.8660254037844389297 ) ) ;
#3971=EDGE_CURVE ( 'NONE', #1249, #1795, #2993, .T. ) ;
#3973=AXIS2_PLACEMENT_3D ( 'NONE', #5317, #2439, #7724 ) ;
#3975=CARTESIAN_POINT ( 'NONE',  ( 33.61000000000001364, 2.449293598294707893E-16, -2.000000000000000888 ) ) ;
#3987=COLOUR_RGB ( '', 0.40784314, 0.44705882, 0.49803922) ;
#4021=DIRECTION ( 'NONE',  ( -0.5000000000000061062, 1.060575238724902601E-16, -0.8660254037844351549 ) ) ;
#4032=CARTESIAN_POINT ( 'NONE',  ( 0.000000000000000000, 0.000000000000000000, 0.000000000000000000 ) ) ;
#4060=EDGE_CURVE ( 'NONE', #3439, #3910, #6480, .T. ) ;
#4067=CARTESIAN_POINT ( 'NONE',  ( 4.200000000000001954, 0.000000000000000000, 0.000000000000000000 ) ) ;
#4069=DIRECTION ( 'NONE',  ( -1.000000000000000000, -0.000000000000000000, -0.000000000000000000 ) ) ;
#4075=DIRECTION ( 'NONE',  ( 0.000000000000000000, -0.5000000000000011102, -0.8660254037844379305 ) ) ;
#4078=ORIENTED_EDGE ( 'NONE', *, *, #2678, .T. ) ;
#4090=CARTESIAN_POINT ( 'NONE',  ( 4.000000000000000000, 0.000000000000000000, 0.000000000000000000 ) ) ;
#4111=ORIENTED_EDGE ( 'NONE', *, *, #2963, .F. ) ;
#4115=AXIS2_PLACEMENT_3D ( 'NONE', #5978, #8054, #7391 ) ;
#4122=ORIENTED_EDGE ( 'NONE', *, *, #5202, .T. ) ;
#4146=DIRECTION ( 'NONE',  ( -1.000000000000000000, -0.000000000000000000, -0.000000000000000000 ) ) ;
#4177=ORIENTED_EDGE ( 'NONE', *, *, #4888, .F. ) ;
#4182=EDGE_LOOP ( 'NONE', ( #7335, #2027, #6805, #3831, #7640 ) ) ;
#4187=CARTESIAN_POINT ( 'NONE',  ( 2.000000000000000000, 0.8865213383406717051, 1.535499999999999199 ) ) ;
#4229=CARTESIAN_POINT ( 'NONE',  ( 2.000000000000000000, 1.773042676681340968, -1.951563910473907981E-15 ) ) ;
#4231=EDGE_LOOP ( 'NONE', ( #1140, #4837, #5307, #8402 ) ) ;
#4240=SHAPE_DEFINITION_REPRESENTATION ( #990, #7097 ) ;
#4260=CIRCLE ( 'NONE', #1585, 1.535500000000000087 ) ;
#4263=PLANE ( 'NONE',  #7804 ) ;
#4274=CARTESIAN_POINT ( 'NONE',  ( 0.000000000000000000, 4.163799117101000559E-16, -3.299999999999999822 ) ) ;
#4292=ORIENTED_EDGE ( 'NONE', *, *, #6522, .T. ) ;
#4298=ADVANCED_FACE ( 'NONE', ( #7869 ), #7118, .T. ) ;
#4304=CONICAL_SURFACE ( 'NONE', #1631, 1.535500000000000087, 1.047197551196590748 ) ;
#4326=DIRECTION ( 'NONE',  ( 0.000000000000000000, 0.000000000000000000, -1.000000000000000000 ) ) ;
#4329=LINE ( 'NONE', #7625, #8600 ) ;
#4330=AXIS2_PLACEMENT_3D ( 'NONE', #3914, #2063, #7435 ) ;
#4340=VERTEX_POINT ( 'NONE', #3243 ) ;
#4355=CLOSED_SHELL ( 'NONE', ( #2469, #1232, #5692, #5149, #966, #4465, #606, #6106, #8706, #8561, #5704, #1353, #6759, #3416, #4298, #8603, #3716, #413, #929, #7051, #5600, #5855, #3262, #4504, #1274, #2736, #6072 ) ) ;
#4369=PLANE ( 'NONE',  #3885 ) ;
#4371=VECTOR ( 'NONE', #1821, 1000.000000000000000 ) ;
#4380=CARTESIAN_POINT ( 'NONE',  ( 0.1999999999999987899, 0.000000000000000000, 3.500000000000000000 ) ) ;
#4383=SURFACE_SIDE_STYLE ('',( #1693 ) ) ;
#4405=LINE ( 'NONE', #8466, #6646 ) ;
#4411=CIRCLE ( 'NONE', #3570, 0.2000000000000000944 ) ;
#4420=DIRECTION ( 'NONE',  ( 0.000000000000000000, 0.000000000000000000, 1.000000000000000000 ) ) ;
#4446=DIRECTION ( 'NONE',  ( 0.000000000000000000, -0.5000000000000011102, -0.8660254037844379305 ) ) ;
#4448=CARTESIAN_POINT ( 'NONE',  ( 2.000000000000000000, 0.000000000000000000, 0.000000000000000000 ) ) ;
#4457=AXIS2_PLACEMENT_3D ( 'NONE', #5158, #2849, #2188 ) ;
#4464=AXIS2_PLACEMENT_3D ( 'NONE', #6745, #4069, #6791 ) ;
#4465=ADVANCED_FACE ( 'NONE', ( #6008 ), #8698, .T. ) ;
#4471=UNCERTAINTY_MEASURE_WITH_UNIT (LENGTH_MEASURE( 1.000000000000000082E-05 ), #7559, 'distance_accuracy_value', 'NONE');
#4488=DIRECTION ( 'NONE',  ( 0.000000000000000000, 0.000000000000000000, -1.000000000000000000 ) ) ;
#4497=EDGE_CURVE ( 'NONE', #899, #6389, #135, .T. ) ;
#4503=CARTESIAN_POINT ( 'NONE',  ( 0.000000000000000000, 1.773042676681340968, -1.951563910473907981E-15 ) ) ;
#4504=ADVANCED_FACE ( 'NONE', ( #6710 ), #532, .F. ) ;
#4531=DIRECTION ( 'NONE',  ( -1.000000000000000000, -0.000000000000000000, -0.000000000000000000 ) ) ;
#4569=EDGE_CURVE ( 'NONE', #4798, #5904, #1286, .T. ) ;
#4579=ORIENTED_EDGE ( 'NONE', *, *, #6310, .T. ) ;
#4594=VERTEX_POINT ( 'NONE', #8354 ) ;
#4611=VECTOR ( 'NONE', #6654, 1000.000000000000114 ) ;
#4613=VERTEX_POINT ( 'NONE', #2977 ) ;
#4644=ADVANCED_BREP_SHAPE_REPRESENTATION ( '', ( #2959, #2554 ), #7620 ) ;
#4661=VERTEX_POINT ( 'NONE', #6272 ) ;
#4664=EDGE_CURVE ( 'NONE', #4613, #5875, #6606, .T. ) ;
#4665=CYLINDRICAL_SURFACE ( 'NONE', #3973, 3.500000000000000000 ) ;
#4666=EDGE_LOOP ( 'NONE', ( #6042, #942, #22 ) ) ;
#4688=VECTOR ( 'NONE', #4446, 1000.000000000000114 ) ;
#4689=EDGE_CURVE ( 'NONE', #5629, #8625, #7750, .T. ) ;
#4694=AXIS2_PLACEMENT_3D ( 'NONE', #5485, #3560, #6244 ) ;
#4698=CARTESIAN_POINT ( 'NONE',  ( 2.000000000000000000, 0.8865213383406717051, 1.535499999999999199 ) ) ;
#4715=ORIENTED_EDGE ( 'NONE', *, *, #4664, .T. ) ;
#4725=FACE_OUTER_BOUND ( 'NONE', #166, .T. ) ;
#4737=CARTESIAN_POINT ( 'NONE',  ( 2.000000000000000000, -0.8865213383406692627, 1.535500000000001641 ) ) ;
#4770=EDGE_CURVE ( 'NONE', #3552, #3394, #6230, .T. ) ;
#4789=ORIENTED_EDGE ( 'NONE', *, *, #6666, .T. ) ;
#4798=VERTEX_POINT ( 'NONE', #848 ) ;
#4816=DIRECTION ( 'NONE',  ( -1.000000000000000000, -0.000000000000000000, -0.000000000000000000 ) ) ;
#4830=DIRECTION ( 'NONE',  ( 0.000000000000000000, 0.000000000000000000, -1.000000000000000000 ) ) ;
#4836=EDGE_CURVE ( 'NONE', #5393, #8009, #474, .T. ) ;
#4837=ORIENTED_EDGE ( 'NONE', *, *, #2963, .T. ) ;
#4845=EDGE_CURVE ( 'NONE', #8009, #4594, #3675, .T. ) ;
#4853=CARTESIAN_POINT ( 'NONE',  ( 2.000000000000000000, -0.8865213383406692627, 1.535500000000001641 ) ) ;
#4864=ORIENTED_EDGE ( 'NONE', *, *, #6003, .F. ) ;
#4879=ORIENTED_EDGE ( 'NONE', *, *, #7985, .F. ) ;
#4888=EDGE_CURVE ( 'NONE', #4891, #3552, #2444, .T. ) ;
#4891=VERTEX_POINT ( 'NONE', #6444 ) ;
#4915=ORIENTED_EDGE ( 'NONE', *, *, #465, .T. ) ;
#4947=CARTESIAN_POINT ( 'NONE',  ( 2.000000000000000000, -1.773042676681341634, 2.493664996716660198E-15 ) ) ;
#4954=DIRECTION ( 'NONE',  ( 1.000000000000000000, 0.000000000000000000, 0.000000000000000000 ) ) ;
#4958=VERTEX_POINT ( 'NONE', #4380 ) ;
#4988=DIRECTION ( 'NONE',  ( 0.000000000000000000, 0.000000000000000000, -1.000000000000000000 ) ) ;
#5001=ORIENTED_EDGE ( 'NONE', *, *, #1812, .F. ) ;
#5014=CARTESIAN_POINT ( 'NONE',  ( 0.000000000000000000, -1.773042676681341634, 2.493664996716660198E-15 ) ) ;
#5018=ORIENTED_EDGE ( 'NONE', *, *, #1574, .F. ) ;
#5029=UNCERTAINTY_MEASURE_WITH_UNIT (LENGTH_MEASURE( 1.000000000000000082E-05 ), #3763, 'distance_accuracy_value', 'NONE');
#5030=PLANE ( 'NONE',  #2773 ) ;
#5034=VECTOR ( 'NONE', #979, 1000.000000000000000 ) ;
#5055=ORIENTED_EDGE ( 'NONE', *, *, #2548, .T. ) ;
#5082=AXIS2_PLACEMENT_3D ( 'NONE', #3861, #5714, #6456 ) ;
#5084=( NAMED_UNIT ( * ) SI_UNIT ( $, .STERADIAN. ) SOLID_ANGLE_UNIT ( ) );
#5085=EDGE_LOOP ( 'NONE', ( #497, #810, #2115 ) ) ;
#5123=CARTESIAN_POINT ( 'NONE',  ( 0.1999999999999987899, 0.000000000000000000, 0.000000000000000000 ) ) ;
#5127=SHAPE_REPRESENTATION_RELATIONSHIP ( 'NONE' , 'NONE' ,  #7097, #4644 ) ;
#5149=ADVANCED_FACE ( 'NONE', ( #4725 ), #7277, .T. ) ;
#5158=CARTESIAN_POINT ( 'NONE',  ( 0.1999999999999987899, 0.000000000000000000, 0.000000000000000000 ) ) ;
#5202=EDGE_CURVE ( 'NONE', #3178, #4594, #2702, .T. ) ;
#5205=VERTEX_POINT ( 'NONE', #3975 ) ;
#5242=DIRECTION ( 'NONE',  ( -1.000000000000000000, -0.000000000000000000, -0.000000000000000000 ) ) ;
#5252=FACE_OUTER_BOUND ( 'NONE', #6468, .T. ) ;
#5259=CARTESIAN_POINT ( 'NONE',  ( 2.000000000000000000, -1.329782007511006725, -0.7677499999999984892 ) ) ;
#5273=CARTESIAN_POINT ( 'NONE',  ( 0.1999999999999987899, 0.000000000000000000, 0.000000000000000000 ) ) ;
#5290=DIRECTION ( 'NONE',  ( 0.000000000000000000, -0.5000000000000012212, -0.8660254037844380415 ) ) ;
#5300=ORIENTED_EDGE ( 'NONE', *, *, #5775, .F. ) ;
#5307=ORIENTED_EDGE ( 'NONE', *, *, #2621, .T. ) ;
#5317=CARTESIAN_POINT ( 'NONE',  ( -31.74999999999995737, 0.000000000000000000, 0.000000000000000000 ) ) ;
#5339=DIRECTION ( 'NONE',  ( 0.000000000000000000, 0.000000000000000000, 1.000000000000000000 ) ) ;
#5351=CARTESIAN_POINT ( 'NONE',  ( 0.000000000000000000, 0.000000000000000000, 3.299999999999999822 ) ) ;
#5379=CARTESIAN_POINT ( 'NONE',  ( 33.61000000000001364, 0.000000000000000000, 2.000000000000000888 ) ) ;
#5380=DIRECTION ( 'NONE',  ( -1.000000000000000000, -0.000000000000000000, -0.000000000000000000 ) ) ;
#5393=VERTEX_POINT ( 'NONE', #1790 ) ;
#5420=PLANE ( 'NONE',  #1800 ) ;
#5431=ORIENTED_EDGE ( 'NONE', *, *, #6037, .F. ) ;
#5447=EDGE_LOOP ( 'NONE', ( #6774, #6994, #5928, #5901 ) ) ;
#5452=CIRCLE ( 'NONE', #663, 3.500000000000000000 ) ;
#5455=DIRECTION ( 'NONE',  ( -0.000000000000000000, 1.467581828789149532E-15, 1.000000000000000000 ) ) ;
#5468=EDGE_CURVE ( 'NONE', #4891, #4798, #7157, .T. ) ;
#5474=LINE ( 'NONE', #6846, #6942 ) ;
#5485=CARTESIAN_POINT ( 'NONE',  ( 4.000000000000003553, 0.000000000000000000, 0.000000000000000000 ) ) ;
#5486=CARTESIAN_POINT ( 'NONE',  ( -31.74999999999995737, 2.449293598294707893E-16, -2.000000000000000888 ) ) ;
#5511=EDGE_LOOP ( 'NONE', ( #385, #1938, #6722 ) ) ;
#5520=DIRECTION ( 'NONE',  ( 0.000000000000000000, 0.000000000000000000, -1.000000000000000000 ) ) ;
#5545=CIRCLE ( 'NONE', #6955, 2.200000000000001066 ) ;
#5555=PRODUCT_CONTEXT ( 'NONE', #3360, 'mechanical' ) ;
#5561=DIRECTION ( 'NONE',  ( 0.000000000000000000, 1.000000000000000000, -1.467581828789149335E-15 ) ) ;
#5571=ORIENTED_EDGE ( 'NONE', *, *, #7844, .T. ) ;
#5590=AXIS2_PLACEMENT_3D ( 'NONE', #568, #3413, #3281 ) ;
#5600=ADVANCED_FACE ( 'NONE', ( #5252 ), #2623, .F. ) ;
#5612=FACE_OUTER_BOUND ( 'NONE', #3745, .T. ) ;
#5619=PRESENTATION_STYLE_ASSIGNMENT (( #1611 ) ) ;
#5629=VERTEX_POINT ( 'NONE', #1328 ) ;
#5641=UNCERTAINTY_MEASURE_WITH_UNIT (LENGTH_MEASURE( 1.000000000000000082E-05 ), #1028, 'distance_accuracy_value', 'NONE');
#5642=FACE_OUTER_BOUND ( 'NONE', #646, .T. ) ;
#5667=EDGE_CURVE ( 'NONE', #3178, #4798, #1222, .T. ) ;
#5686=ORIENTED_EDGE ( 'NONE', *, *, #7019, .T. ) ;
#5692=ADVANCED_FACE ( 'NONE', ( #3940 ), #376, .F. ) ;
#5694=DIRECTION ( 'NONE',  ( 0.000000000000000000, 0.000000000000000000, 1.000000000000000000 ) ) ;
#5697=DIRECTION ( 'NONE',  ( 0.000000000000000000, -1.000000000000000000, 8.560894001270036306E-16 ) ) ;
#5704=ADVANCED_FACE ( 'NONE', ( #6658 ), #8277, .T. ) ;
#5712=AXIS2_PLACEMENT_3D ( 'NONE', #5273, #3756, #5694 ) ;
#5714=DIRECTION ( 'NONE',  ( 1.000000000000000000, 0.000000000000000000, 0.000000000000000000 ) ) ;
#5758=ORIENTED_EDGE ( 'NONE', *, *, #3928, .T. ) ;
#5765=DIRECTION ( 'NONE',  ( 0.000000000000000000, -1.000000000000000000, 0.000000000000000000 ) ) ;
#5769=ORIENTED_EDGE ( 'NONE', *, *, #2621, .F. ) ;
#5773=ORIENTED_EDGE ( 'NONE', *, *, #4060, .T. ) ;
#5775=EDGE_CURVE ( 'NONE', #1907, #5205, #6155, .T. ) ;
#5783=FACE_OUTER_BOUND ( 'NONE', #2723, .T. ) ;
#5786=( NAMED_UNIT ( * ) SI_UNIT ( $, .STERADIAN. ) SOLID_ANGLE_UNIT ( ) );
#5787=ORIENTED_EDGE ( 'NONE', *, *, #629, .T. ) ;
#5799=PLANE ( 'NONE',  #5082 ) ;
#5812=DIRECTION ( 'NONE',  ( -1.000000000000000000, -0.000000000000000000, -0.000000000000000000 ) ) ;
#5817=AXIS2_PLACEMENT_3D ( 'NONE', #7344, #8710, #7966 ) ;
#5826=DIRECTION ( 'NONE',  ( 0.000000000000000000, 0.000000000000000000, 1.000000000000000000 ) ) ;
#5851=DIRECTION ( 'NONE',  ( 0.000000000000000000, 0.000000000000000000, -1.000000000000000000 ) ) ;
#5855=ADVANCED_FACE ( 'NONE', ( #8691 ), #5420, .F. ) ;
#5875=VERTEX_POINT ( 'NONE', #6613 ) ;
#5881=CIRCLE ( 'NONE', #3634, 2.000000000000000888 ) ;
#5901=ORIENTED_EDGE ( 'NONE', *, *, #428, .F. ) ;
#5904=VERTEX_POINT ( 'NONE', #4947 ) ;
#5922=CARTESIAN_POINT ( 'NONE',  ( 2.000000000000000000, 0.000000000000000000, 0.000000000000000000 ) ) ;
#5928=ORIENTED_EDGE ( 'NONE', *, *, #2305, .T. ) ;
#5932=ORIENTED_EDGE ( 'NONE', *, *, #7811, .F. ) ;
#5938=DIRECTION ( 'NONE',  ( 0.000000000000000000, -0.5000000000000012212, -0.8660254037844380415 ) ) ;
#5964=DIRECTION ( 'NONE',  ( 1.000000000000000000, 0.000000000000000000, 0.000000000000000000 ) ) ;
#5978=CARTESIAN_POINT ( 'NONE',  ( 2.000000000000000000, 0.8865213383406683745, -1.535500000000000753 ) ) ;
#5999=ORIENTED_EDGE ( 'NONE', *, *, #2548, .F. ) ;
#6003=EDGE_CURVE ( 'NONE', #94, #6389, #7205, .T. ) ;
#6008=FACE_OUTER_BOUND ( 'NONE', #3704, .T. ) ;
#6037=EDGE_CURVE ( 'NONE', #4798, #3552, #1155, .T. ) ;
#6042=ORIENTED_EDGE ( 'NONE', *, *, #6870, .T. ) ;
#6062=ORIENTED_EDGE ( 'NONE', *, *, #7316, .F. ) ;
#6072=ADVANCED_FACE ( 'NONE', ( #2355 ), #8344, .F. ) ;
#6082=VECTOR ( 'NONE', #4146, 1000.000000000000000 ) ;
#6088=DIRECTION ( 'NONE',  ( 0.000000000000000000, 0.000000000000000000, -1.000000000000000000 ) ) ;
#6091=AXIS2_PLACEMENT_3D ( 'NONE', #4067, #8126, #6088 ) ;
#6106=ADVANCED_FACE ( 'NONE', ( #3754 ), #4665, .T. ) ;
#6112=DIRECTION ( 'NONE',  ( 0.000000000000000000, 0.5000000000000012212, 0.8660254037844380415 ) ) ;
#6120=DIRECTION ( 'NONE',  ( -1.000000000000000000, -0.000000000000000000, -0.000000000000000000 ) ) ;
#6124=LINE ( 'NONE', #4187, #6082 ) ;
#6129=CIRCLE ( 'NONE', #5712, 3.500000000000000000 ) ;
#6148=ORIENTED_EDGE ( 'NONE', *, *, #7316, .T. ) ;
#6155=CIRCLE ( 'NONE', #5590, 2.000000000000000888 ) ;
#6177=LINE ( 'NONE', #136, #8069 ) ;
#6178=ORIENTED_EDGE ( 'NONE', *, *, #3043, .T. ) ;
#6194=VECTOR ( 'NONE', #7504, 1000.000000000000114 ) ;
#6198=LINE ( 'NONE', #5486, #1361 ) ;
#6202=ORIENTED_EDGE ( 'NONE', *, *, #612, .T. ) ;
#6230=LINE ( 'NONE', #2846, #3946 ) ;
#6236=VECTOR ( 'NONE', #1132, 1000.000000000000000 ) ;
#6244=DIRECTION ( 'NONE',  ( 0.000000000000000000, 0.000000000000000000, 1.000000000000000000 ) ) ;
#6272=CARTESIAN_POINT ( 'NONE',  ( 4.000000000000003553, 4.286263797015736595E-16, -3.500000000000000000 ) ) ;
#6275=DIRECTION ( 'NONE',  ( 0.000000000000000000, 0.5000000000000011102, 0.8660254037844379305 ) ) ;
#6293=LINE ( 'NONE', #2871, #7140 ) ;
#6294=CARTESIAN_POINT ( 'NONE',  ( 2.000000000000000000, 0.000000000000000000, 0.000000000000000000 ) ) ;
#6310=EDGE_CURVE ( 'NONE', #7760, #8009, #4260, .T. ) ;
#6327=PLANE ( 'NONE',  #7894 ) ;
#6329=EDGE_CURVE ( 'NONE', #3439, #7760, #216, .T. ) ;
#6335=AXIS2_PLACEMENT_3D ( 'NONE', #4032, #7953, #6578 ) ;
#6339=DIRECTION ( 'NONE',  ( 0.000000000000000000, 0.000000000000000000, 1.000000000000000000 ) ) ;
#6376=EDGE_CURVE ( 'NONE', #3394, #1209, #6124, .T. ) ;
#6389=VERTEX_POINT ( 'NONE', #4274 ) ;
#6392=CARTESIAN_POINT ( 'NONE',  ( 0.000000000000000000, -0.8865213383406692627, 1.535500000000001641 ) ) ;
#6397=DIRECTION ( 'NONE',  ( 0.000000000000000000, 1.224646799147353207E-16, 1.000000000000000000 ) ) ;
#6440=AXIS2_PLACEMENT_3D ( 'NONE', #610, #1320, #2614 ) ;
#6444=CARTESIAN_POINT ( 'NONE',  ( 2.000000000000000000, -0.8865213383406692627, 1.535500000000001641 ) ) ;
#6456=DIRECTION ( 'NONE',  ( 0.000000000000000000, 0.000000000000000000, -1.000000000000000000 ) ) ;
#6468=EDGE_LOOP ( 'NONE', ( #2507, #3650, #7557 ) ) ;
#6479=DIRECTION ( 'NONE',  ( -0.000000000000000000, 0.000000000000000000, 1.000000000000000000 ) ) ;
#6480=LINE ( 'NONE', #7815, #1686 ) ;
#6522=EDGE_CURVE ( 'NONE', #4594, #1795, #4405, .T. ) ;
#6525=CIRCLE ( 'NONE', #6091, 2.000000000000000888 ) ;
#6553=ORIENTED_EDGE ( 'NONE', *, *, #7973, .F. ) ;
#6565=DIRECTION ( 'NONE',  ( 0.000000000000000000, 1.000000000000000000, -1.224646799147353207E-16 ) ) ;
#6570=ORIENTED_EDGE ( 'NONE', *, *, #4664, .F. ) ;
#6578=DIRECTION ( 'NONE',  ( 0.000000000000000000, 0.000000000000000000, 1.000000000000000000 ) ) ;
#6587=ORIENTED_EDGE ( 'NONE', *, *, #3395, .F. ) ;
#6606=CIRCLE ( 'NONE', #8461, 2.000000000000000888 ) ;
#6610=LINE ( 'NONE', #7367, #7636 ) ;
#6613=CARTESIAN_POINT ( 'NONE',  ( 4.200000000000001954, 2.449293598294707893E-16, -2.000000000000000888 ) ) ;
#6634=ORIENTED_EDGE ( 'NONE', *, *, #7673, .T. ) ;
#6646=VECTOR ( 'NONE', #5812, 1000.000000000000000 ) ;
#6651=AXIS2_PLACEMENT_3D ( 'NONE', #3336, #2717, #4830 ) ;
#6654=DIRECTION ( 'NONE',  ( 0.000000000000000000, 0.4999999999999989453, -0.8660254037844392627 ) ) ;
#6658=FACE_OUTER_BOUND ( 'NONE', #5447, .T. ) ;
#6666=EDGE_CURVE ( 'NONE', #1476, #7760, #1734, .T. ) ;
#6686=CARTESIAN_POINT ( 'NONE',  ( 2.000000000000000000, 0.000000000000000000, 0.000000000000000000 ) ) ;
#6708=DIRECTION ( 'NONE',  ( 0.000000000000000000, 0.000000000000000000, -1.000000000000000000 ) ) ;
#6710=FACE_OUTER_BOUND ( 'NONE', #5511, .T. ) ;
#6721=VECTOR ( 'NONE', #6867, 1000.000000000000000 ) ;
#6722=ORIENTED_EDGE ( 'NONE', *, *, #6881, .F. ) ;
#6724=FACE_OUTER_BOUND ( 'NONE', #4666, .T. ) ;
#6725=FACE_OUTER_BOUND ( 'NONE', #8675, .T. ) ;
#6745=CARTESIAN_POINT ( 'NONE',  ( 34.00000000000000000, 0.000000000000000000, 0.000000000000000000 ) ) ;
#6750=DIRECTION ( 'NONE',  ( 1.000000000000000000, 0.000000000000000000, 0.000000000000000000 ) ) ;
#6759=ADVANCED_FACE ( 'NONE', ( #7754 ), #8215, .F. ) ;
#6764=CYLINDRICAL_SURFACE ( 'NONE', #4330, 2.000000000000000888 ) ;
#6774=ORIENTED_EDGE ( 'NONE', *, *, #3928, .F. ) ;
#6780=DIRECTION ( 'NONE',  ( -1.000000000000000000, -0.000000000000000000, -0.000000000000000000 ) ) ;
#6791=DIRECTION ( 'NONE',  ( 0.000000000000000000, 0.000000000000000000, 1.000000000000000000 ) ) ;
#6805=ORIENTED_EDGE ( 'NONE', *, *, #2080, .T. ) ;
#6812=EDGE_LOOP ( 'NONE', ( #5932, #152, #2981, #5571, #3052 ) ) ;
#6829=VECTOR ( 'NONE', #7265, 1000.000000000000114 ) ;
#6846=CARTESIAN_POINT ( 'NONE',  ( 2.000000000000000000, -1.773042676681341634, 2.493664996716660198E-15 ) ) ;
#6858=DIRECTION ( 'NONE',  ( 0.000000000000000000, 0.000000000000000000, 1.000000000000000000 ) ) ;
#6867=DIRECTION ( 'NONE',  ( -1.000000000000000000, -0.000000000000000000, -0.000000000000000000 ) ) ;
#6870=EDGE_CURVE ( 'NONE', #7760, #5393, #8107, .T. ) ;
#6878=ORIENTED_EDGE ( 'NONE', *, *, #4845, .F. ) ;
#6881=EDGE_CURVE ( 'NONE', #3552, #1476, #1447, .T. ) ;
#6897=FILL_AREA_STYLE_COLOUR ( '', #3987 ) ;
#6901=CARTESIAN_POINT ( 'NONE',  ( 4.000000000000000000, 0.000000000000000000, 0.000000000000000000 ) ) ;
#6919=PRODUCT_DEFINITION_FORMATION_WITH_SPECIFIED_SOURCE ( 'ANY', '', #1628, .NOT_KNOWN. ) ;
#6931=VECTOR ( 'NONE', #1906, 1000.000000000000227 ) ;
#6942=VECTOR ( 'NONE', #7426, 1000.000000000000114 ) ;
#6955=AXIS2_PLACEMENT_3D ( 'NONE', #6901, #2113, #2287 ) ;
#6990=DIRECTION ( 'NONE',  ( 0.000000000000000000, 0.000000000000000000, 1.000000000000000000 ) ) ;
#6994=ORIENTED_EDGE ( 'NONE', *, *, #4689, .T. ) ;
#6998=AXIS2_PLACEMENT_3D ( 'NONE', #5123, #394, #1633 ) ;
#7013=CARTESIAN_POINT ( 'NONE',  ( 0.000000000000000000, 0.8865213383406683745, -1.535500000000000753 ) ) ;
#7019=EDGE_CURVE ( 'NONE', #4340, #1975, #587, .T. ) ;
#7026=EDGE_CURVE ( 'NONE', #1975, #4340, #5545, .T. ) ;
#7038=VERTEX_POINT ( 'NONE', #1441 ) ;
#7048=ORIENTED_EDGE ( 'NONE', *, *, #7899, .F. ) ;
#7051=ADVANCED_FACE ( 'NONE', ( #69 ), #4263, .F. ) ;
#7079=AXIS2_PLACEMENT_3D ( 'NONE', #4448, #3089, #6339 ) ;
#7085=ORIENTED_EDGE ( 'NONE', *, *, #5468, .F. ) ;
#7097=SHAPE_REPRESENTATION ( 'socket head cap screw_iso_ISO 4762 M4 x 30 - 20N', ( #2554 ), #7620 ) ;
#7110=ORIENTED_EDGE ( 'NONE', *, *, #4569, .T. ) ;
#7118=PLANE ( 'NONE',  #1123 ) ;
#7131=AXIS2_PLACEMENT_3D ( 'NONE', #1557, #898, #6275 ) ;
#7132=DIRECTION ( 'NONE',  ( 1.000000000000000000, 0.000000000000000000, 0.000000000000000000 ) ) ;
#7136=AXIS2_PLACEMENT_3D ( 'NONE', #3240, #6750, #6708 ) ;
#7140=VECTOR ( 'NONE', #6120, 1000.000000000000000 ) ;
#7147=CARTESIAN_POINT ( 'NONE',  ( 2.000000000000000000, 0.8865213383406683745, -1.535500000000000753 ) ) ;
#7157=LINE ( 'NONE', #3034, #2645 ) ;
#7171=LINE ( 'NONE', #7215, #6236 ) ;
#7191=DIRECTION ( 'NONE',  ( 0.000000000000000000, -0.4999999999999992784, 0.8660254037844389297 ) ) ;
#7205=CIRCLE ( 'NONE', #3417, 0.2000000000000000944 ) ;
#7215=CARTESIAN_POINT ( 'NONE',  ( -31.74999999999995737, 0.000000000000000000, 3.500000000000000000 ) ) ;
#7228=VECTOR ( 'NONE', #3078, 1000.000000000000000 ) ;
#7229=APPLICATION_CONTEXT ( 'automotive_design' ) ;
#7257=FACE_OUTER_BOUND ( 'NONE', #322, .T. ) ;
#7264=ORIENTED_EDGE ( 'NONE', *, *, #428, .T. ) ;
#7265=DIRECTION ( 'NONE',  ( -0.7071067811865355823, 0.000000000000000000, 0.7071067811865595631 ) ) ;
#7277=CONICAL_SURFACE ( 'NONE', #6440, 1.610000000000000098, 0.7853981633974652654 ) ;
#7305=ORIENTED_EDGE ( 'NONE', *, *, #8599, .T. ) ;
#7316=EDGE_CURVE ( 'NONE', #1907, #4613, #3037, .T. ) ;
#7335=ORIENTED_EDGE ( 'NONE', *, *, #8697, .F. ) ;
#7341=ORIENTED_EDGE ( 'NONE', *, *, #8287, .F. ) ;
#7344=CARTESIAN_POINT ( 'NONE',  ( 2.000000000000000000, 1.773042676681340968, -1.951563910473907981E-15 ) ) ;
#7353=AXIS2_PLACEMENT_3D ( 'NONE', #8173, #4816, #1461 ) ;
#7355=CARTESIAN_POINT ( 'NONE',  ( 2.000000000000000000, 1.773042676681340968, -1.951563910473907981E-15 ) ) ;
#7367=CARTESIAN_POINT ( 'NONE',  ( 2.000000000000000000, 1.773042676681340968, -1.951563910473907981E-15 ) ) ;
#7383=CARTESIAN_POINT ( 'NONE',  ( 0.1999999999999987899, 0.000000000000000000, 3.299999999999999822 ) ) ;
#7387=ORIENTED_EDGE ( 'NONE', *, *, #7985, .T. ) ;
#7391=DIRECTION ( 'NONE',  ( 0.000000000000000000, 1.000000000000000000, -8.560894001270036306E-16 ) ) ;
#7395=ORIENTED_EDGE ( 'NONE', *, *, #1071, .T. ) ;
#7426=DIRECTION ( 'NONE',  ( 0.000000000000000000, 0.4999999999999989453, -0.8660254037844392627 ) ) ;
#7431=CIRCLE ( 'NONE', #8147, 0.2000000000000000944 ) ;
#7435=DIRECTION ( 'NONE',  ( 0.000000000000000000, 0.000000000000000000, 1.000000000000000000 ) ) ;
#7465=CARTESIAN_POINT ( 'NONE',  ( 4.200000000000001954, 0.000000000000000000, 0.000000000000000000 ) ) ;
#7475=PLANE ( 'NONE',  #5817 ) ;
#7503=CARTESIAN_POINT ( 'NONE',  ( 2.000000000000000000, 0.000000000000000000, 0.000000000000000000 ) ) ;
#7504=DIRECTION ( 'NONE',  ( -0.7071067811865355823, 8.659560562355079537E-17, -0.7071067811865595631 ) ) ;
#7536=FACE_OUTER_BOUND ( 'NONE', #7593, .T. ) ;
#7557=ORIENTED_EDGE ( 'NONE', *, *, #2080, .F. ) ;
#7559=( LENGTH_UNIT ( ) NAMED_UNIT ( * ) SI_UNIT ( .MILLI., .METRE. ) );
#7576=EDGE_LOOP ( 'NONE', ( #7658, #4879, #5055, #3817 ) ) ;
#7580=PRODUCT_DEFINITION_CONTEXT ( 'detailed design', #7229, 'design' ) ;
#7593=EDGE_LOOP ( 'NONE', ( #510, #2118 ) ) ;
#7620=( GEOMETRIC_REPRESENTATION_CONTEXT ( 3 ) GLOBAL_UNCERTAINTY_ASSIGNED_CONTEXT ( ( #5641 ) ) GLOBAL_UNIT_ASSIGNED_CONTEXT ( ( #1028, #3154, #5084 ) ) REPRESENTATION_CONTEXT ( 'NONE', 'WORKASPACE' ) );
#7625=CARTESIAN_POINT ( 'NONE',  ( 0.000000000000000000, -0.8865213383406692627, 1.535500000000001641 ) ) ;
#7631=CARTESIAN_POINT ( 'NONE',  ( 4.000000000000001776, 2.694222958124178486E-16, 2.200000000000001066 ) ) ;
#7636=VECTOR ( 'NONE', #7191, 1000.000000000000227 ) ;
#7639=CARTESIAN_POINT ( 'NONE',  ( 2.000000000000000000, 2.253471898105739434E-15, 1.535500000000000309 ) ) ;
#7640=ORIENTED_EDGE ( 'NONE', *, *, #6037, .T. ) ;
#7658=ORIENTED_EDGE ( 'NONE', *, *, #465, .F. ) ;
#7673=EDGE_CURVE ( 'NONE', #8625, #5629, #2737, .T. ) ;
#7716=ORIENTED_EDGE ( 'NONE', *, *, #8287, .T. ) ;
#7719=CARTESIAN_POINT ( 'NONE',  ( 2.000000000000000000, 1.773042676681340968, -1.951563910473907981E-15 ) ) ;
#7724=DIRECTION ( 'NONE',  ( 0.000000000000000000, 0.000000000000000000, 1.000000000000000000 ) ) ;
#7750=CIRCLE ( 'NONE', #844, 1.610000000000000098 ) ;
#7754=FACE_OUTER_BOUND ( 'NONE', #7576, .T. ) ;
#7760=VERTEX_POINT ( 'NONE', #2144 ) ;
#7763=DIRECTION ( 'NONE',  ( 0.000000000000000000, 1.000000000000000000, -1.467581828789149335E-15 ) ) ;
#7771=CARTESIAN_POINT ( 'NONE',  ( 2.000000000000000000, 0.8865213383406683745, -1.535500000000000753 ) ) ;
#7773=FILL_AREA_STYLE ('',( #2980 ) ) ;
#7787=CARTESIAN_POINT ( 'NONE',  ( 0.000000000000000000, 0.000000000000000000, 0.000000000000000000 ) ) ;
#7804=AXIS2_PLACEMENT_3D ( 'NONE', #730, #3437, #6112 ) ;
#7811=EDGE_CURVE ( 'NONE', #3910, #1209, #1948, .T. ) ;
#7813=DIRECTION ( 'NONE',  ( 0.000000000000000000, -0.4999999999999989453, 0.8660254037844391517 ) ) ;
#7815=CARTESIAN_POINT ( 'NONE',  ( 2.000000000000000000, 1.773042676681340968, -1.951563910473907981E-15 ) ) ;
#7844=EDGE_CURVE ( 'NONE', #1476, #3394, #6610, .T. ) ;
#7860=ORIENTED_EDGE ( 'NONE', *, *, #1, .F. ) ;
#7869=FACE_OUTER_BOUND ( 'NONE', #6812, .T. ) ;
#7873=EDGE_LOOP ( 'NONE', ( #4864, #5018, #2366, #783 ) ) ;
#7888=AXIS2_PLACEMENT_3D ( 'NONE', #3901, #1957, #2625 ) ;
#7894=AXIS2_PLACEMENT_3D ( 'NONE', #1314, #5455, #1359 ) ;
#7895=PLANE ( 'NONE',  #2515 ) ;
#7899=EDGE_CURVE ( 'NONE', #344, #8009, #704, .T. ) ;
#7905=MECHANICAL_DESIGN_GEOMETRIC_PRESENTATION_REPRESENTATION('',(#722),#1432);
#7930=CARTESIAN_POINT ( 'NONE',  ( 34.00000000000000000, 0.000000000000000000, 1.610000000000000098 ) ) ;
#7949=CARTESIAN_POINT ( 'NONE',  ( 0.000000000000000000, 1.773042676681340968, -1.951563910473907981E-15 ) ) ;
#7953=DIRECTION ( 'NONE',  ( -1.000000000000000000, -0.000000000000000000, -0.000000000000000000 ) ) ;
#7966=DIRECTION ( 'NONE',  ( 0.000000000000000000, 0.000000000000000000, -1.000000000000000000 ) ) ;
#7973=EDGE_CURVE ( 'NONE', #2290, #1795, #6177, .T. ) ;
#7985=EDGE_CURVE ( 'NONE', #5875, #4613, #6525, .T. ) ;
#8009=VERTEX_POINT ( 'NONE', #750 ) ;
#8050=EDGE_LOOP ( 'NONE', ( #7085, #65, #5431 ) ) ;
#8054=DIRECTION ( 'NONE',  ( 0.000000000000000000, -8.560894001270036306E-16, -1.000000000000000000 ) ) ;
#8069=VECTOR ( 'NONE', #839, 1000.000000000000000 ) ;
#8070=FACE_OUTER_BOUND ( 'NONE', #297, .T. ) ;
#8083=DIRECTION ( 'NONE',  ( 0.000000000000000000, 0.000000000000000000, -1.000000000000000000 ) ) ;
#8107=LINE ( 'NONE', #1932, #3283 ) ;
#8126=DIRECTION ( 'NONE',  ( 1.000000000000000000, 0.000000000000000000, 0.000000000000000000 ) ) ;
#8129=CARTESIAN_POINT ( 'NONE',  ( 2.000000000000000000, 1.773042676681340968, -1.951563910473907981E-15 ) ) ;
#8147=AXIS2_PLACEMENT_3D ( 'NONE', #1107, #6565, #6397 ) ;
#8173=CARTESIAN_POINT ( 'NONE',  ( 2.000000000000000000, 0.000000000000000000, 0.000000000000000000 ) ) ;
#8209=DIRECTION ( 'NONE',  ( 0.000000000000000000, -0.5000000000000012212, -0.8660254037844380415 ) ) ;
#8215=TOROIDAL_SURFACE ( 'NONE', #737, 2.200000000000001066, 0.2000000000000000111 ) ;
#8271=PLANE ( 'NONE',  #7131 ) ;
#8277=CONICAL_SURFACE ( 'NONE', #4464, 1.610000000000000098, 0.7853981633974652654 ) ;
#8287=EDGE_CURVE ( 'NONE', #8357, #1209, #4329, .T. ) ;
#8292=CARTESIAN_POINT ( 'NONE',  ( 0.1999999999999987899, 4.286263797015736595E-16, -3.500000000000000000 ) ) ;
#8295=CARTESIAN_POINT ( 'NONE',  ( 2.000000000000000000, 0.000000000000000000, 0.000000000000000000 ) ) ;
#8324=DIRECTION ( 'NONE',  ( 0.000000000000000000, 0.000000000000000000, -1.000000000000000000 ) ) ;
#8342=DIRECTION ( 'NONE',  ( 1.000000000000000000, 0.000000000000000000, 0.000000000000000000 ) ) ;
#8344=CONICAL_SURFACE ( 'NONE', #439, 1.535500000000000087, 1.047197551196590748 ) ;
#8354=CARTESIAN_POINT ( 'NONE',  ( 2.000000000000000000, -0.8865213383406729264, -1.535499999999999421 ) ) ;
#8356=SURFACE_STYLE_USAGE ( .BOTH. , #4383 ) ;
#8357=VERTEX_POINT ( 'NONE', #6392 ) ;
#8366=DIRECTION ( 'NONE',  ( 0.000000000000000000, -0.5000000000000011102, -0.8660254037844379305 ) ) ;
#8372=ORIENTED_EDGE ( 'NONE', *, *, #2126, .T. ) ;
#8385=ORIENTED_EDGE ( 'NONE', *, *, #6003, .T. ) ;
#8402=ORIENTED_EDGE ( 'NONE', *, *, #1574, .T. ) ;
#8420=EDGE_LOOP ( 'NONE', ( #1852, #7264, #6148, #4715 ) ) ;
#8461=AXIS2_PLACEMENT_3D ( 'NONE', #7465, #4954, #5520 ) ;
#8466=CARTESIAN_POINT ( 'NONE',  ( 2.000000000000000000, -0.8865213383406729264, -1.535499999999999421 ) ) ;
#8510=ORIENTED_EDGE ( 'NONE', *, *, #6522, .F. ) ;
#8561=ADVANCED_FACE ( 'NONE', ( #248 ), #2949, .T. ) ;
#8599=EDGE_CURVE ( 'NONE', #4661, #94, #1985, .T. ) ;
#8600=VECTOR ( 'NONE', #7763, 1000.000000000000000 ) ;
#8601=CARTESIAN_POINT ( 'NONE',  ( 0.000000000000000000, 0.000000000000000000, 0.000000000000000000 ) ) ;
#8603=ADVANCED_FACE ( 'NONE', ( #8070 ), #6327, .F. ) ;
#8612=CARTESIAN_POINT ( 'NONE',  ( 0.000000000000000000, -0.8865213383406729264, -1.535499999999999421 ) ) ;
#8625=VERTEX_POINT ( 'NONE', #2127 ) ;
#8632=CARTESIAN_POINT ( 'NONE',  ( 2.000000000000000000, 0.000000000000000000, 0.000000000000000000 ) ) ;
#8675=EDGE_LOOP ( 'NONE', ( #1296, #8510, #6878, #1213, #2430 ) ) ;
#8677=ORIENTED_EDGE ( 'NONE', *, *, #5775, .T. ) ;
#8691=FACE_OUTER_BOUND ( 'NONE', #5085, .T. ) ;
#8697=EDGE_CURVE ( 'NONE', #344, #3552, #3734, .T. ) ;
#8698=CYLINDRICAL_SURFACE ( 'NONE', #7888, 3.500000000000000000 ) ;
#8706=ADVANCED_FACE ( 'NONE', ( #1041, #292 ), #5799, .T. ) ;
#8710=DIRECTION ( 'NONE',  ( 1.000000000000000000, 0.000000000000000000, 0.000000000000000000 ) ) ;
ENDSEC;
END-ISO-10303-21;
